ISO-10303-21;
HEADER;
/* Generated by software containing ST-Developer
 * from STEP Tools, Inc. (www.steptools.com) 
 */

FILE_DESCRIPTION(
/* description */ (''),
/* implementation_level */ '2;1');

FILE_NAME(
/* name */ '14_DIN_3760_A_25x40x7_NBR_Lip_Seal.step',
/* time_stamp */ '2026-10-23T00:52:27+05:00',
/* author */ (''),
/* organization */ (''),
/* preprocessor_version */ 'ST-DEVELOPER v20.2',
/* originating_system */ 'Autodesk Translation Framework v15.15.0.0',
/* authorisation */ '');

FILE_SCHEMA (('AUTOMOTIVE_DESIGN { 1 0 10303 214 3 1 1 }'));
ENDSEC;

DATA;
#10=MECHANICAL_DESIGN_GEOMETRIC_PRESENTATION_REPRESENTATION('',(#1553),#59204);
#1513=SHAPE_REPRESENTATION_RELATIONSHIP('SRR','None',#59302,#1533);
#1533=ADVANCED_BREP_SHAPE_REPRESENTATION('',(#1580),#59189);
#1553=STYLED_ITEM('',(#59593),#1580);
#1580=MANIFOLD_SOLID_BREP('Lip seal',#22809);
#1624=FACE_BOUND('',#4075,.T.);
#1625=FACE_BOUND('',#4077,.T.);
#1626=FACE_BOUND('',#4081,.T.);
#1627=FACE_BOUND('',#4084,.T.);
#1628=FACE_BOUND('',#4093,.T.);
#1831=PLANE('',#23198);
#1832=PLANE('',#23199);
#1833=PLANE('',#23208);
#1834=PLANE('',#23211);
#1835=PLANE('',#23227);
#2427=CYLINDRICAL_SURFACE('',#23192,1.9);
#2428=CYLINDRICAL_SURFACE('',#23195,1.7);
#2429=CYLINDRICAL_SURFACE('',#23205,2.);
#2430=CYLINDRICAL_SURFACE('',#23213,1.65);
#2431=CYLINDRICAL_SURFACE('',#23215,1.4);
#2432=CYLINDRICAL_SURFACE('',#23219,1.55);
#2433=CYLINDRICAL_SURFACE('',#23223,1.25);
#2742=FACE_OUTER_BOUND('',#4072,.T.);
#2743=FACE_OUTER_BOUND('',#4073,.T.);
#2744=FACE_OUTER_BOUND('',#4074,.T.);
#2745=FACE_OUTER_BOUND('',#4076,.T.);
#2746=FACE_OUTER_BOUND('',#4078,.T.);
#2747=FACE_OUTER_BOUND('',#4079,.T.);
#2748=FACE_OUTER_BOUND('',#4080,.T.);
#2749=FACE_OUTER_BOUND('',#4082,.T.);
#2750=FACE_OUTER_BOUND('',#4083,.T.);
#2751=FACE_OUTER_BOUND('',#4085,.T.);
#2752=FACE_OUTER_BOUND('',#4086,.T.);
#2753=FACE_OUTER_BOUND('',#4087,.T.);
#2754=FACE_OUTER_BOUND('',#4088,.T.);
#2755=FACE_OUTER_BOUND('',#4089,.T.);
#2756=FACE_OUTER_BOUND('',#4090,.T.);
#2757=FACE_OUTER_BOUND('',#4091,.T.);
#2758=FACE_OUTER_BOUND('',#4092,.T.);
#4072=EDGE_LOOP('',(#14976,#14977,#14978,#14979));
#4073=EDGE_LOOP('',(#14980,#14981,#14982,#14983));
#4074=EDGE_LOOP('',(#14984));
#4075=EDGE_LOOP('',(#14985));
#4076=EDGE_LOOP('',(#14986));
#4077=EDGE_LOOP('',(#14987));
#4078=EDGE_LOOP('',(#14988,#14989,#14990,#14991,#14992));
#4079=EDGE_LOOP('',(#14993,#14994,#14995,#14996,#14997,#14998));
#4080=EDGE_LOOP('',(#14999));
#4081=EDGE_LOOP('',(#15000));
#4082=EDGE_LOOP('',(#15001,#15002,#15003,#15004,#15005));
#4083=EDGE_LOOP('',(#15006));
#4084=EDGE_LOOP('',(#15007));
#4085=EDGE_LOOP('',(#15008,#15009,#15010,#15011));
#4086=EDGE_LOOP('',(#15012,#15013,#15014,#15015));
#4087=EDGE_LOOP('',(#15016,#15017,#15018,#15019));
#4088=EDGE_LOOP('',(#15020,#15021,#15022,#15023));
#4089=EDGE_LOOP('',(#15024,#15025,#15026,#15027));
#4090=EDGE_LOOP('',(#15028,#15029,#15030,#15031));
#4091=EDGE_LOOP('',(#15032,#15033,#15034,#15035));
#4092=EDGE_LOOP('',(#15036));
#4093=EDGE_LOOP('',(#15037));
#5562=LINE('',#32233,#6995);
#5563=LINE('',#32239,#6996);
#5564=LINE('',#32249,#6997);
#5565=LINE('',#32255,#6998);
#5566=LINE('',#32262,#6999);
#5567=LINE('',#32270,#7000);
#5568=LINE('',#32273,#7001);
#5569=LINE('',#32277,#7002);
#5570=LINE('',#32281,#7003);
#5571=LINE('',#32285,#7004);
#5572=LINE('',#32289,#7005);
#5573=LINE('',#32293,#7006);
#6995=VECTOR('',#25486,1.9);
#6996=VECTOR('',#25493,1.7);
#6997=VECTOR('',#25506,1.98);
#6998=VECTOR('',#25513,2.);
#6999=VECTOR('',#25522,1.98);
#7000=VECTOR('',#25533,1.65);
#7001=VECTOR('',#25536,1.4);
#7002=VECTOR('',#25541,1.475);
#7003=VECTOR('',#25546,1.55);
#7004=VECTOR('',#25551,1.4);
#7005=VECTOR('',#25556,1.25);
#7006=VECTOR('',#25561,1.4);
#8427=CIRCLE('',#23193,1.9);
#8428=CIRCLE('',#23194,1.9);
#8429=CIRCLE('',#23196,1.7);
#8430=CIRCLE('',#23197,1.7);
#8431=CIRCLE('',#23200,1.4);
#8432=CIRCLE('',#23202,1.96);
#8433=CIRCLE('',#23203,2.);
#8434=CIRCLE('',#23204,2.);
#8435=CIRCLE('',#23206,2.);
#8436=CIRCLE('',#23207,2.);
#8437=CIRCLE('',#23210,1.96);
#8438=CIRCLE('',#23212,1.65);
#8439=CIRCLE('',#23214,1.65);
#8440=CIRCLE('',#23216,1.4);
#8441=CIRCLE('',#23218,1.55);
#8442=CIRCLE('',#23220,1.55);
#8443=CIRCLE('',#23222,1.25);
#8444=CIRCLE('',#23224,1.25);
#8445=CIRCLE('',#23226,1.55);
#9287=VERTEX_POINT('',#32230);
#9288=VERTEX_POINT('',#32232);
#9289=VERTEX_POINT('',#32236);
#9290=VERTEX_POINT('',#32238);
#9291=VERTEX_POINT('',#32243);
#9292=VERTEX_POINT('',#32246);
#9293=VERTEX_POINT('',#32248);
#9294=VERTEX_POINT('',#32250);
#9295=VERTEX_POINT('',#32254);
#9296=VERTEX_POINT('',#32256);
#9297=VERTEX_POINT('',#32261);
#9298=VERTEX_POINT('',#32265);
#9299=VERTEX_POINT('',#32268);
#9300=VERTEX_POINT('',#32272);
#9301=VERTEX_POINT('',#32276);
#9302=VERTEX_POINT('',#32280);
#9303=VERTEX_POINT('',#32284);
#9304=VERTEX_POINT('',#32288);
#9305=VERTEX_POINT('',#32292);
#11492=EDGE_CURVE('',#9287,#9287,#8427,.T.);
#11493=EDGE_CURVE('',#9287,#9288,#5562,.T.);
#11494=EDGE_CURVE('',#9288,#9288,#8428,.T.);
#11495=EDGE_CURVE('',#9289,#9289,#8429,.T.);
#11496=EDGE_CURVE('',#9289,#9290,#5563,.T.);
#11497=EDGE_CURVE('',#9290,#9290,#8430,.T.);
#11498=EDGE_CURVE('',#9291,#9291,#8431,.T.);
#11499=EDGE_CURVE('',#9292,#9292,#8432,.T.);
#11500=EDGE_CURVE('',#9292,#9293,#5564,.T.);
#11501=EDGE_CURVE('',#9293,#9294,#8433,.T.);
#11502=EDGE_CURVE('',#9294,#9293,#8434,.T.);
#11503=EDGE_CURVE('',#9294,#9295,#5565,.T.);
#11504=EDGE_CURVE('',#9296,#9295,#8435,.T.);
#11505=EDGE_CURVE('',#9295,#9296,#8436,.T.);
#11506=EDGE_CURVE('',#9296,#9297,#5566,.T.);
#11507=EDGE_CURVE('',#9297,#9297,#8437,.T.);
#11508=EDGE_CURVE('',#9298,#9298,#8438,.T.);
#11509=EDGE_CURVE('',#9299,#9299,#8439,.T.);
#11510=EDGE_CURVE('',#9299,#9298,#5567,.T.);
#11511=EDGE_CURVE('',#9291,#9300,#5568,.T.);
#11512=EDGE_CURVE('',#9300,#9300,#8440,.T.);
#11513=EDGE_CURVE('',#9300,#9301,#5569,.T.);
#11514=EDGE_CURVE('',#9301,#9301,#8441,.T.);
#11515=EDGE_CURVE('',#9301,#9302,#5570,.T.);
#11516=EDGE_CURVE('',#9302,#9302,#8442,.T.);
#11517=EDGE_CURVE('',#9302,#9303,#5571,.T.);
#11518=EDGE_CURVE('',#9303,#9303,#8443,.T.);
#11519=EDGE_CURVE('',#9303,#9304,#5572,.T.);
#11520=EDGE_CURVE('',#9304,#9304,#8444,.T.);
#11521=EDGE_CURVE('',#9304,#9305,#5573,.T.);
#11522=EDGE_CURVE('',#9305,#9305,#8445,.T.);
#14976=ORIENTED_EDGE('',*,*,#11492,.F.);
#14977=ORIENTED_EDGE('',*,*,#11493,.T.);
#14978=ORIENTED_EDGE('',*,*,#11494,.F.);
#14979=ORIENTED_EDGE('',*,*,#11493,.F.);
#14980=ORIENTED_EDGE('',*,*,#11495,.T.);
#14981=ORIENTED_EDGE('',*,*,#11496,.T.);
#14982=ORIENTED_EDGE('',*,*,#11497,.F.);
#14983=ORIENTED_EDGE('',*,*,#11496,.F.);
#14984=ORIENTED_EDGE('',*,*,#11492,.T.);
#14985=ORIENTED_EDGE('',*,*,#11495,.F.);
#14986=ORIENTED_EDGE('',*,*,#11497,.T.);
#14987=ORIENTED_EDGE('',*,*,#11498,.F.);
#14988=ORIENTED_EDGE('',*,*,#11499,.T.);
#14989=ORIENTED_EDGE('',*,*,#11500,.T.);
#14990=ORIENTED_EDGE('',*,*,#11501,.T.);
#14991=ORIENTED_EDGE('',*,*,#11502,.T.);
#14992=ORIENTED_EDGE('',*,*,#11500,.F.);
#14993=ORIENTED_EDGE('',*,*,#11501,.F.);
#14994=ORIENTED_EDGE('',*,*,#11502,.F.);
#14995=ORIENTED_EDGE('',*,*,#11503,.T.);
#14996=ORIENTED_EDGE('',*,*,#11504,.F.);
#14997=ORIENTED_EDGE('',*,*,#11505,.F.);
#14998=ORIENTED_EDGE('',*,*,#11503,.F.);
#14999=ORIENTED_EDGE('',*,*,#11499,.F.);
#15000=ORIENTED_EDGE('',*,*,#11494,.T.);
#15001=ORIENTED_EDGE('',*,*,#11504,.T.);
#15002=ORIENTED_EDGE('',*,*,#11505,.T.);
#15003=ORIENTED_EDGE('',*,*,#11506,.T.);
#15004=ORIENTED_EDGE('',*,*,#11507,.T.);
#15005=ORIENTED_EDGE('',*,*,#11506,.F.);
#15006=ORIENTED_EDGE('',*,*,#11507,.F.);
#15007=ORIENTED_EDGE('',*,*,#11508,.T.);
#15008=ORIENTED_EDGE('',*,*,#11509,.T.);
#15009=ORIENTED_EDGE('',*,*,#11510,.T.);
#15010=ORIENTED_EDGE('',*,*,#11508,.F.);
#15011=ORIENTED_EDGE('',*,*,#11510,.F.);
#15012=ORIENTED_EDGE('',*,*,#11498,.T.);
#15013=ORIENTED_EDGE('',*,*,#11511,.T.);
#15014=ORIENTED_EDGE('',*,*,#11512,.F.);
#15015=ORIENTED_EDGE('',*,*,#11511,.F.);
#15016=ORIENTED_EDGE('',*,*,#11512,.T.);
#15017=ORIENTED_EDGE('',*,*,#11513,.T.);
#15018=ORIENTED_EDGE('',*,*,#11514,.F.);
#15019=ORIENTED_EDGE('',*,*,#11513,.F.);
#15020=ORIENTED_EDGE('',*,*,#11514,.T.);
#15021=ORIENTED_EDGE('',*,*,#11515,.T.);
#15022=ORIENTED_EDGE('',*,*,#11516,.F.);
#15023=ORIENTED_EDGE('',*,*,#11515,.F.);
#15024=ORIENTED_EDGE('',*,*,#11516,.T.);
#15025=ORIENTED_EDGE('',*,*,#11517,.T.);
#15026=ORIENTED_EDGE('',*,*,#11518,.F.);
#15027=ORIENTED_EDGE('',*,*,#11517,.F.);
#15028=ORIENTED_EDGE('',*,*,#11518,.T.);
#15029=ORIENTED_EDGE('',*,*,#11519,.T.);
#15030=ORIENTED_EDGE('',*,*,#11520,.F.);
#15031=ORIENTED_EDGE('',*,*,#11519,.F.);
#15032=ORIENTED_EDGE('',*,*,#11520,.T.);
#15033=ORIENTED_EDGE('',*,*,#11521,.T.);
#15034=ORIENTED_EDGE('',*,*,#11522,.F.);
#15035=ORIENTED_EDGE('',*,*,#11521,.F.);
#15036=ORIENTED_EDGE('',*,*,#11509,.F.);
#15037=ORIENTED_EDGE('',*,*,#11522,.T.);
#21344=CONICAL_SURFACE('',#23201,1.98,0.785398163397448);
#21345=CONICAL_SURFACE('',#23209,1.98,0.785398163397448);
#21346=CONICAL_SURFACE('',#23217,1.475,1.13416916698136);
#21347=CONICAL_SURFACE('',#23221,1.4,1.24904577239825);
#21348=CONICAL_SURFACE('',#23225,1.4,1.13416916698136);
#21572=ADVANCED_FACE('',(#2742),#2427,.F.);
#21573=ADVANCED_FACE('',(#2743),#2428,.T.);
#21574=ADVANCED_FACE('',(#2744,#1624),#1831,.F.);
#21575=ADVANCED_FACE('',(#2745,#1625),#1832,.T.);
#21576=ADVANCED_FACE('',(#2746),#21344,.T.);
#21577=ADVANCED_FACE('',(#2747),#2429,.T.);
#21578=ADVANCED_FACE('',(#2748,#1626),#1833,.T.);
#21579=ADVANCED_FACE('',(#2749),#21345,.T.);
#21580=ADVANCED_FACE('',(#2750,#1627),#1834,.T.);
#21581=ADVANCED_FACE('',(#2751),#2430,.F.);
#21582=ADVANCED_FACE('',(#2752),#2431,.F.);
#21583=ADVANCED_FACE('',(#2753),#21346,.F.);
#21584=ADVANCED_FACE('',(#2754),#2432,.F.);
#21585=ADVANCED_FACE('',(#2755),#21347,.F.);
#21586=ADVANCED_FACE('',(#2756),#2433,.F.);
#21587=ADVANCED_FACE('',(#2757),#21348,.F.);
#21588=ADVANCED_FACE('',(#2758,#1628),#1835,.T.);
#22809=CLOSED_SHELL('',(#21572,#21573,#21574,#21575,#21576,#21577,#21578,
#21579,#21580,#21581,#21582,#21583,#21584,#21585,#21586,#21587,#21588));
#23191=AXIS2_PLACEMENT_3D('',#32228,#25480,#25481);
#23192=AXIS2_PLACEMENT_3D('',#32229,#25482,#25483);
#23193=AXIS2_PLACEMENT_3D('',#32231,#25484,#25485);
#23194=AXIS2_PLACEMENT_3D('',#32234,#25487,#25488);
#23195=AXIS2_PLACEMENT_3D('',#32235,#25489,#25490);
#23196=AXIS2_PLACEMENT_3D('',#32237,#25491,#25492);
#23197=AXIS2_PLACEMENT_3D('',#32240,#25494,#25495);
#23198=AXIS2_PLACEMENT_3D('',#32241,#25496,#25497);
#23199=AXIS2_PLACEMENT_3D('',#32242,#25498,#25499);
#23200=AXIS2_PLACEMENT_3D('',#32244,#25500,#25501);
#23201=AXIS2_PLACEMENT_3D('',#32245,#25502,#25503);
#23202=AXIS2_PLACEMENT_3D('',#32247,#25504,#25505);
#23203=AXIS2_PLACEMENT_3D('',#32251,#25507,#25508);
#23204=AXIS2_PLACEMENT_3D('',#32252,#25509,#25510);
#23205=AXIS2_PLACEMENT_3D('',#32253,#25511,#25512);
#23206=AXIS2_PLACEMENT_3D('',#32257,#25514,#25515);
#23207=AXIS2_PLACEMENT_3D('',#32258,#25516,#25517);
#23208=AXIS2_PLACEMENT_3D('',#32259,#25518,#25519);
#23209=AXIS2_PLACEMENT_3D('',#32260,#25520,#25521);
#23210=AXIS2_PLACEMENT_3D('',#32263,#25523,#25524);
#23211=AXIS2_PLACEMENT_3D('',#32264,#25525,#25526);
#23212=AXIS2_PLACEMENT_3D('',#32266,#25527,#25528);
#23213=AXIS2_PLACEMENT_3D('',#32267,#25529,#25530);
#23214=AXIS2_PLACEMENT_3D('',#32269,#25531,#25532);
#23215=AXIS2_PLACEMENT_3D('',#32271,#25534,#25535);
#23216=AXIS2_PLACEMENT_3D('',#32274,#25537,#25538);
#23217=AXIS2_PLACEMENT_3D('',#32275,#25539,#25540);
#23218=AXIS2_PLACEMENT_3D('',#32278,#25542,#25543);
#23219=AXIS2_PLACEMENT_3D('',#32279,#25544,#25545);
#23220=AXIS2_PLACEMENT_3D('',#32282,#25547,#25548);
#23221=AXIS2_PLACEMENT_3D('',#32283,#25549,#25550);
#23222=AXIS2_PLACEMENT_3D('',#32286,#25552,#25553);
#23223=AXIS2_PLACEMENT_3D('',#32287,#25554,#25555);
#23224=AXIS2_PLACEMENT_3D('',#32290,#25557,#25558);
#23225=AXIS2_PLACEMENT_3D('',#32291,#25559,#25560);
#23226=AXIS2_PLACEMENT_3D('',#32294,#25562,#25563);
#23227=AXIS2_PLACEMENT_3D('',#32295,#25564,#25565);
#25480=DIRECTION('axis',(0.,0.,1.));
#25481=DIRECTION('refdir',(1.,0.,0.));
#25482=DIRECTION('center_axis',(0.,0.,1.));
#25483=DIRECTION('ref_axis',(1.,0.,0.));
#25484=DIRECTION('center_axis',(0.,0.,1.));
#25485=DIRECTION('ref_axis',(1.,0.,0.));
#25486=DIRECTION('',(0.,0.,1.));
#25487=DIRECTION('center_axis',(0.,0.,-1.));
#25488=DIRECTION('ref_axis',(1.,0.,0.));
#25489=DIRECTION('center_axis',(0.,0.,1.));
#25490=DIRECTION('ref_axis',(1.,0.,0.));
#25491=DIRECTION('center_axis',(0.,0.,1.));
#25492=DIRECTION('ref_axis',(1.,0.,0.));
#25493=DIRECTION('',(0.,0.,1.));
#25494=DIRECTION('center_axis',(0.,0.,1.));
#25495=DIRECTION('ref_axis',(1.,0.,0.));
#25496=DIRECTION('center_axis',(0.,0.,-1.));
#25497=DIRECTION('ref_axis',(-1.,0.,0.));
#25498=DIRECTION('center_axis',(0.,0.,1.));
#25499=DIRECTION('ref_axis',(1.,0.,0.));
#25500=DIRECTION('center_axis',(0.,0.,1.));
#25501=DIRECTION('ref_axis',(1.,0.,0.));
#25502=DIRECTION('center_axis',(0.,0.,-1.));
#25503=DIRECTION('ref_axis',(-1.,0.,0.));
#25504=DIRECTION('center_axis',(0.,0.,-1.));
#25505=DIRECTION('ref_axis',(-1.,0.,0.));
#25506=DIRECTION('',(0.707106781186548,8.65956056235493E-17,-0.707106781186548));
#25507=DIRECTION('center_axis',(0.,0.,1.));
#25508=DIRECTION('ref_axis',(-1.,0.,0.));
#25509=DIRECTION('center_axis',(0.,0.,1.));
#25510=DIRECTION('ref_axis',(-1.,0.,0.));
#25511=DIRECTION('center_axis',(0.,0.,1.));
#25512=DIRECTION('ref_axis',(1.,0.,0.));
#25513=DIRECTION('',(0.,0.,-1.));
#25514=DIRECTION('center_axis',(0.,0.,-1.));
#25515=DIRECTION('ref_axis',(-1.,0.,0.));
#25516=DIRECTION('center_axis',(0.,0.,-1.));
#25517=DIRECTION('ref_axis',(-1.,0.,0.));
#25518=DIRECTION('center_axis',(0.,0.,1.));
#25519=DIRECTION('ref_axis',(1.,0.,0.));
#25520=DIRECTION('center_axis',(0.,0.,1.));
#25521=DIRECTION('ref_axis',(-1.,0.,0.));
#25522=DIRECTION('',(-0.707106781186548,-8.65956056235493E-17,-0.707106781186548));
#25523=DIRECTION('center_axis',(0.,0.,1.));
#25524=DIRECTION('ref_axis',(-1.,0.,0.));
#25525=DIRECTION('center_axis',(0.,0.,-1.));
#25526=DIRECTION('ref_axis',(-1.,0.,0.));
#25527=DIRECTION('center_axis',(0.,0.,1.));
#25528=DIRECTION('ref_axis',(1.,0.,0.));
#25529=DIRECTION('center_axis',(0.,0.,1.));
#25530=DIRECTION('ref_axis',(1.,0.,0.));
#25531=DIRECTION('center_axis',(0.,0.,1.));
#25532=DIRECTION('ref_axis',(1.,0.,0.));
#25533=DIRECTION('',(0.,0.,-1.));
#25534=DIRECTION('center_axis',(0.,0.,1.));
#25535=DIRECTION('ref_axis',(1.,0.,0.));
#25536=DIRECTION('',(0.,0.,-1.));
#25537=DIRECTION('center_axis',(0.,0.,1.));
#25538=DIRECTION('ref_axis',(1.,0.,0.));
#25539=DIRECTION('center_axis',(0.,0.,-1.));
#25540=DIRECTION('ref_axis',(1.,0.,0.));
#25541=DIRECTION('',(-0.906183139995265,-1.1097542818365E-16,-0.422885465331124));
#25542=DIRECTION('center_axis',(0.,0.,1.));
#25543=DIRECTION('ref_axis',(1.,0.,0.));
#25544=DIRECTION('center_axis',(0.,0.,1.));
#25545=DIRECTION('ref_axis',(1.,0.,0.));
#25546=DIRECTION('',(0.,0.,-1.));
#25547=DIRECTION('center_axis',(0.,0.,1.));
#25548=DIRECTION('ref_axis',(1.,0.,0.));
#25549=DIRECTION('center_axis',(0.,0.,1.));
#25550=DIRECTION('ref_axis',(1.,0.,0.));
#25551=DIRECTION('',(0.948683298050514,1.16180196436212E-16,-0.316227766016838));
#25552=DIRECTION('center_axis',(0.,0.,1.));
#25553=DIRECTION('ref_axis',(1.,0.,0.));
#25554=DIRECTION('center_axis',(0.,0.,1.));
#25555=DIRECTION('ref_axis',(1.,0.,0.));
#25556=DIRECTION('',(0.,0.,-1.));
#25557=DIRECTION('center_axis',(0.,0.,1.));
#25558=DIRECTION('ref_axis',(1.,0.,0.));
#25559=DIRECTION('center_axis',(0.,0.,-1.));
#25560=DIRECTION('ref_axis',(1.,0.,0.));
#25561=DIRECTION('',(-0.906183139995265,-1.1097542818365E-16,-0.422885465331124));
#25562=DIRECTION('center_axis',(0.,0.,1.));
#25563=DIRECTION('ref_axis',(1.,0.,0.));
#25564=DIRECTION('center_axis',(0.,0.,-1.));
#25565=DIRECTION('ref_axis',(-1.,0.,0.));
#32228=CARTESIAN_POINT('',(0.,0.,0.));
#32229=CARTESIAN_POINT('Origin',(0.,0.,0.68));
#32230=CARTESIAN_POINT('',(-1.9,-2.32682891837997E-16,0.66));
#32231=CARTESIAN_POINT('Origin',(0.,0.,0.66));
#32232=CARTESIAN_POINT('',(-1.9,-2.32682891837997E-16,0.7));
#32233=CARTESIAN_POINT('',(-1.9,-2.32682891837997E-16,0.68));
#32234=CARTESIAN_POINT('Origin',(0.,0.,0.7));
#32235=CARTESIAN_POINT('Origin',(0.,0.,0.68));
#32236=CARTESIAN_POINT('',(-1.7,-2.0818995585505E-16,0.66));
#32237=CARTESIAN_POINT('Origin',(0.,0.,0.66));
#32238=CARTESIAN_POINT('',(-1.7,-2.0818995585505E-16,0.7));
#32239=CARTESIAN_POINT('',(-1.7,-2.0818995585505E-16,0.68));
#32240=CARTESIAN_POINT('Origin',(0.,0.,0.7));
#32241=CARTESIAN_POINT('Origin',(1.9,0.,0.66));
#32242=CARTESIAN_POINT('Origin',(1.4,0.,0.7));
#32243=CARTESIAN_POINT('',(-1.4,-1.71450551880629E-16,0.7));
#32244=CARTESIAN_POINT('Origin',(0.,0.,0.7));
#32245=CARTESIAN_POINT('Origin',(0.,0.,0.68));
#32246=CARTESIAN_POINT('',(1.96,-2.40030772632881E-16,0.7));
#32247=CARTESIAN_POINT('Origin',(0.,0.,0.7));
#32248=CARTESIAN_POINT('',(2.,2.44929359829471E-16,0.66));
#32249=CARTESIAN_POINT('',(1.98,2.42480066231176E-16,0.68));
#32250=CARTESIAN_POINT('',(-2.,-2.44929359829471E-16,0.66));
#32251=CARTESIAN_POINT('Origin',(0.,0.,0.66));
#32252=CARTESIAN_POINT('Origin',(0.,0.,0.66));
#32253=CARTESIAN_POINT('Origin',(0.,0.,0.35));
#32254=CARTESIAN_POINT('',(-2.,-2.44929359829471E-16,0.04));
#32255=CARTESIAN_POINT('',(-2.,-2.44929359829471E-16,0.35));
#32256=CARTESIAN_POINT('',(2.,-2.44929359829471E-16,0.04));
#32257=CARTESIAN_POINT('Origin',(0.,0.,0.04));
#32258=CARTESIAN_POINT('Origin',(0.,0.,0.04));
#32259=CARTESIAN_POINT('Origin',(1.4,0.,0.7));
#32260=CARTESIAN_POINT('Origin',(0.,0.,0.02));
#32261=CARTESIAN_POINT('',(1.96,2.40030772632881E-16,0.));
#32262=CARTESIAN_POINT('',(1.98,2.42480066231176E-16,0.02));
#32263=CARTESIAN_POINT('Origin',(0.,0.,0.));
#32264=CARTESIAN_POINT('Origin',(2.,0.,0.));
#32265=CARTESIAN_POINT('',(-1.65,-2.02066721859313E-16,6.93889390390723E-18));
#32266=CARTESIAN_POINT('Origin',(0.,0.,0.));
#32267=CARTESIAN_POINT('Origin',(0.,0.,0.06));
#32268=CARTESIAN_POINT('',(-1.65,-2.02066721859313E-16,0.12));
#32269=CARTESIAN_POINT('Origin',(0.,0.,0.12));
#32270=CARTESIAN_POINT('',(-1.65,-2.02066721859313E-16,0.06));
#32271=CARTESIAN_POINT('Origin',(0.,0.,0.665));
#32272=CARTESIAN_POINT('',(-1.4,-1.71450551880629E-16,0.63));
#32273=CARTESIAN_POINT('',(-1.4,-1.71450551880629E-16,0.665));
#32274=CARTESIAN_POINT('Origin',(0.,0.,0.63));
#32275=CARTESIAN_POINT('Origin',(0.,0.,0.595));
#32276=CARTESIAN_POINT('',(-1.55,-1.8982025386784E-16,0.56));
#32277=CARTESIAN_POINT('',(-1.475,-1.80635402874235E-16,0.595));
#32278=CARTESIAN_POINT('Origin',(0.,0.,0.56));
#32279=CARTESIAN_POINT('Origin',(0.,0.,0.49));
#32280=CARTESIAN_POINT('',(-1.55,-1.8982025386784E-16,0.42));
#32281=CARTESIAN_POINT('',(-1.55,-1.8982025386784E-16,0.49));
#32282=CARTESIAN_POINT('Origin',(0.,0.,0.42));
#32283=CARTESIAN_POINT('Origin',(0.,0.,0.37));
#32284=CARTESIAN_POINT('',(-1.25,-1.53080849893419E-16,0.32));
#32285=CARTESIAN_POINT('',(-1.4,-1.71450551880629E-16,0.37));
#32286=CARTESIAN_POINT('Origin',(0.,0.,0.32));
#32287=CARTESIAN_POINT('Origin',(0.,0.,0.29));
#32288=CARTESIAN_POINT('',(-1.25,-1.53080849893419E-16,0.26));
#32289=CARTESIAN_POINT('',(-1.25,-1.53080849893419E-16,0.29));
#32290=CARTESIAN_POINT('Origin',(0.,0.,0.26));
#32291=CARTESIAN_POINT('Origin',(0.,0.,0.19));
#32292=CARTESIAN_POINT('',(-1.55,-1.8982025386784E-16,0.12));
#32293=CARTESIAN_POINT('',(-1.4,-1.71450551880629E-16,0.19));
#32294=CARTESIAN_POINT('Origin',(0.,0.,0.12));
#32295=CARTESIAN_POINT('Origin',(1.65,0.,0.12));
#59167=UNCERTAINTY_MEASURE_WITH_UNIT(LENGTH_MEASURE(0.001),#59205,
'DISTANCE_ACCURACY_VALUE',
'Maximum model space distance between geometric entities at asserted c
onnectivities');
#59182=UNCERTAINTY_MEASURE_WITH_UNIT(LENGTH_MEASURE(0.001),#59205,
'DISTANCE_ACCURACY_VALUE',
'Maximum model space distance between geometric entities at asserted c
onnectivities');
#59189=(
GEOMETRIC_REPRESENTATION_CONTEXT(3)
GLOBAL_UNCERTAINTY_ASSIGNED_CONTEXT((#59167))
GLOBAL_UNIT_ASSIGNED_CONTEXT((#59205,#59207,#59208))
REPRESENTATION_CONTEXT('','3D')
);
#59204=(
GEOMETRIC_REPRESENTATION_CONTEXT(3)
GLOBAL_UNCERTAINTY_ASSIGNED_CONTEXT((#59182))
GLOBAL_UNIT_ASSIGNED_CONTEXT((#59205,#59207,#59208))
REPRESENTATION_CONTEXT('','3D')
);
#59205=(
LENGTH_UNIT()
NAMED_UNIT(*)
SI_UNIT(.CENTI.,.METRE.)
);
#59207=(
NAMED_UNIT(*)
PLANE_ANGLE_UNIT()
SI_UNIT($,.RADIAN.)
);
#59208=(
NAMED_UNIT(*)
SI_UNIT($,.STERADIAN.)
SOLID_ANGLE_UNIT()
);
#59215=SHAPE_DEFINITION_REPRESENTATION(#59236,#59302);
#59236=PRODUCT_DEFINITION_SHAPE('',$,#59324);
#59302=SHAPE_REPRESENTATION('',(#23191),#59189);
#59317=PRODUCT_DEFINITION_CONTEXT('part definition',#59382,'design');
#59324=PRODUCT_DEFINITION('2026-10-23-00-47-22-996',
'14_DIN_3760_A_25x40x7_NBR_Lip_Seal',#59345,#59317);
#59345=PRODUCT_DEFINITION_FORMATION('',$,#59390);
#59382=APPLICATION_CONTEXT(
'Core Data for Automotive Mechanical Design Process');
#59383=PRODUCT_CONTEXT('part definition',#59382,'mechanical');
#59390=PRODUCT('2026-10-23-00-47-22-996',
'14_DIN_3760_A_25x40x7_NBR_Lip_Seal',$,(#59383));
#59587=COLOUR_RGB('Black',0.12,0.14,0.17);
#59588=FILL_AREA_STYLE_COLOUR('',#59587);
#59589=FILL_AREA_STYLE('',(#59588));
#59590=SURFACE_STYLE_FILL_AREA(#59589);
#59591=SURFACE_SIDE_STYLE('',(#59590));
#59592=SURFACE_STYLE_USAGE(.BOTH.,#59591);
#59593=PRESENTATION_STYLE_ASSIGNMENT((#59592));
ENDSEC;
END-ISO-10303-21;
